ISO-10303-21;
HEADER;
/* Generated by software containing ST-Developer
 * from STEP Tools, Inc. (www.steptools.com) 
 */

FILE_DESCRIPTION(
/* description */ ('Shaft runout checking stand'),
/* implementation_level */ '2;1');

FILE_NAME(
/* name */ 'Dead axle (2).step',
/* time_stamp */ '2026-11-02T21:12:33-08:00',
/* author */ (''),
/* organization */ (''),
/* preprocessor_version */ 'ST-DEVELOPER v20.2',
/* originating_system */ 'Autodesk Translation Framework v15.17.0.0',
/* authorisation */ '');

FILE_SCHEMA (('AUTOMOTIVE_DESIGN { 1 0 10303 214 3 1 1 }'));
ENDSEC;

DATA;
#10=MECHANICAL_DESIGN_GEOMETRIC_PRESENTATION_REPRESENTATION('',(#479),#11748);
#393=SHAPE_REPRESENTATION_RELATIONSHIP('SRR','None',#11942,#436);
#436=ADVANCED_BREP_SHAPE_REPRESENTATION('',(#529),#11718);
#479=STYLED_ITEM('',(#12169),#529);
#529=MANIFOLD_SOLID_BREP('Body1',#6223);
#622=FACE_BOUND('',#1643,.T.);
#623=FACE_BOUND('',#1648,.T.);
#767=CIRCLE('',#7024,0.165);
#768=CIRCLE('',#7025,0.165);
#769=CIRCLE('',#7028,0.8);
#770=CIRCLE('',#7029,0.5);
#771=CIRCLE('',#7031,0.8);
#772=CIRCLE('',#7034,0.5);
#982=CYLINDRICAL_SURFACE('',#7023,0.165);
#983=CYLINDRICAL_SURFACE('',#7030,0.8);
#984=CYLINDRICAL_SURFACE('',#7033,0.5);
#1212=FACE_OUTER_BOUND('',#1640,.T.);
#1213=FACE_OUTER_BOUND('',#1641,.T.);
#1214=FACE_OUTER_BOUND('',#1642,.T.);
#1215=FACE_OUTER_BOUND('',#1644,.T.);
#1216=FACE_OUTER_BOUND('',#1645,.T.);
#1217=FACE_OUTER_BOUND('',#1646,.T.);
#1218=FACE_OUTER_BOUND('',#1647,.T.);
#1640=EDGE_LOOP('',(#4896,#4897,#4898,#4899));
#1641=EDGE_LOOP('',(#4900));
#1642=EDGE_LOOP('',(#4901));
#1643=EDGE_LOOP('',(#4902));
#1644=EDGE_LOOP('',(#4903,#4904,#4905,#4906));
#1645=EDGE_LOOP('',(#4907));
#1646=EDGE_LOOP('',(#4908,#4909,#4910,#4911));
#1647=EDGE_LOOP('',(#4912));
#1648=EDGE_LOOP('',(#4913));
#2193=LINE('',#10344,#2660);
#2194=LINE('',#10354,#2661);
#2195=LINE('',#10360,#2662);
#2660=VECTOR('',#8382,0.165);
#2661=VECTOR('',#8395,0.8);
#2662=VECTOR('',#8404,0.5);
#3087=VERTEX_POINT('',#10341);
#3088=VERTEX_POINT('',#10343);
#3089=VERTEX_POINT('',#10348);
#3090=VERTEX_POINT('',#10350);
#3091=VERTEX_POINT('',#10353);
#3092=VERTEX_POINT('',#10358);
#3734=EDGE_CURVE('',#3087,#3087,#767,.T.);
#3735=EDGE_CURVE('',#3087,#3088,#2193,.T.);
#3736=EDGE_CURVE('',#3088,#3088,#768,.T.);
#3737=EDGE_CURVE('',#3089,#3089,#769,.T.);
#3738=EDGE_CURVE('',#3090,#3090,#770,.T.);
#3739=EDGE_CURVE('',#3089,#3091,#2194,.T.);
#3740=EDGE_CURVE('',#3091,#3091,#771,.T.);
#3741=EDGE_CURVE('',#3092,#3092,#772,.T.);
#3742=EDGE_CURVE('',#3092,#3090,#2195,.T.);
#4896=ORIENTED_EDGE('',*,*,#3734,.F.);
#4897=ORIENTED_EDGE('',*,*,#3735,.T.);
#4898=ORIENTED_EDGE('',*,*,#3736,.F.);
#4899=ORIENTED_EDGE('',*,*,#3735,.F.);
#4900=ORIENTED_EDGE('',*,*,#3734,.T.);
#4901=ORIENTED_EDGE('',*,*,#3737,.T.);
#4902=ORIENTED_EDGE('',*,*,#3738,.F.);
#4903=ORIENTED_EDGE('',*,*,#3737,.F.);
#4904=ORIENTED_EDGE('',*,*,#3739,.T.);
#4905=ORIENTED_EDGE('',*,*,#3740,.T.);
#4906=ORIENTED_EDGE('',*,*,#3739,.F.);
#4907=ORIENTED_EDGE('',*,*,#3740,.F.);
#4908=ORIENTED_EDGE('',*,*,#3741,.F.);
#4909=ORIENTED_EDGE('',*,*,#3742,.T.);
#4910=ORIENTED_EDGE('',*,*,#3738,.T.);
#4911=ORIENTED_EDGE('',*,*,#3742,.F.);
#4912=ORIENTED_EDGE('',*,*,#3741,.T.);
#4913=ORIENTED_EDGE('',*,*,#3736,.T.);
#5730=PLANE('',#7026);
#5731=PLANE('',#7027);
#5732=PLANE('',#7032);
#5733=PLANE('',#7035);
#6012=ADVANCED_FACE('',(#1212),#982,.F.);
#6013=ADVANCED_FACE('',(#1213),#5730,.T.);
#6014=ADVANCED_FACE('',(#1214,#622),#5731,.T.);
#6015=ADVANCED_FACE('',(#1215),#983,.T.);
#6016=ADVANCED_FACE('',(#1216),#5732,.F.);
#6017=ADVANCED_FACE('',(#1217),#984,.T.);
#6018=ADVANCED_FACE('',(#1218,#623),#5733,.T.);
#6223=CLOSED_SHELL('',(#6012,#6013,#6014,#6015,#6016,#6017,#6018));
#7022=AXIS2_PLACEMENT_3D('',#10339,#8376,#8377);
#7023=AXIS2_PLACEMENT_3D('',#10340,#8378,#8379);
#7024=AXIS2_PLACEMENT_3D('',#10342,#8380,#8381);
#7025=AXIS2_PLACEMENT_3D('',#10345,#8383,#8384);
#7026=AXIS2_PLACEMENT_3D('',#10346,#8385,#8386);
#7027=AXIS2_PLACEMENT_3D('',#10347,#8387,#8388);
#7028=AXIS2_PLACEMENT_3D('',#10349,#8389,#8390);
#7029=AXIS2_PLACEMENT_3D('',#10351,#8391,#8392);
#7030=AXIS2_PLACEMENT_3D('',#10352,#8393,#8394);
#7031=AXIS2_PLACEMENT_3D('',#10355,#8396,#8397);
#7032=AXIS2_PLACEMENT_3D('',#10356,#8398,#8399);
#7033=AXIS2_PLACEMENT_3D('',#10357,#8400,#8401);
#7034=AXIS2_PLACEMENT_3D('',#10359,#8402,#8403);
#7035=AXIS2_PLACEMENT_3D('',#10361,#8405,#8406);
#8376=DIRECTION('axis',(0.,0.,1.));
#8377=DIRECTION('refdir',(1.,0.,0.));
#8378=DIRECTION('center_axis',(0.,1.,0.));
#8379=DIRECTION('ref_axis',(1.,0.,0.));
#8380=DIRECTION('center_axis',(0.,1.,0.));
#8381=DIRECTION('ref_axis',(1.,0.,0.));
#8382=DIRECTION('',(0.,1.,0.));
#8383=DIRECTION('center_axis',(0.,-1.,0.));
#8384=DIRECTION('ref_axis',(1.,0.,0.));
#8385=DIRECTION('center_axis',(0.,1.,0.));
#8386=DIRECTION('ref_axis',(1.,0.,0.));
#8387=DIRECTION('center_axis',(0.,1.,0.));
#8388=DIRECTION('ref_axis',(1.,0.,0.));
#8389=DIRECTION('center_axis',(0.,1.,0.));
#8390=DIRECTION('ref_axis',(1.,0.,0.));
#8391=DIRECTION('center_axis',(0.,1.,0.));
#8392=DIRECTION('ref_axis',(1.,0.,0.));
#8393=DIRECTION('center_axis',(0.,1.,0.));
#8394=DIRECTION('ref_axis',(1.,0.,0.));
#8395=DIRECTION('',(0.,-1.,0.));
#8396=DIRECTION('center_axis',(0.,1.,0.));
#8397=DIRECTION('ref_axis',(1.,0.,0.));
#8398=DIRECTION('center_axis',(0.,1.,0.));
#8399=DIRECTION('ref_axis',(1.,0.,0.));
#8400=DIRECTION('center_axis',(0.,1.,0.));
#8401=DIRECTION('ref_axis',(1.,0.,0.));
#8402=DIRECTION('center_axis',(0.,1.,0.));
#8403=DIRECTION('ref_axis',(1.,0.,0.));
#8404=DIRECTION('',(0.,-1.,0.));
#8405=DIRECTION('center_axis',(0.,1.,0.));
#8406=DIRECTION('ref_axis',(1.,0.,0.));
#10339=CARTESIAN_POINT('',(0.,0.,0.));
#10340=CARTESIAN_POINT('Origin',(-2.,9.6,5.));
#10341=CARTESIAN_POINT('',(-2.165,9.6,5.));
#10342=CARTESIAN_POINT('Origin',(-2.,9.6,5.));
#10343=CARTESIAN_POINT('',(-2.165,10.8,5.));
#10344=CARTESIAN_POINT('',(-2.165,9.6,5.));
#10345=CARTESIAN_POINT('Origin',(-2.,10.8,5.));
#10346=CARTESIAN_POINT('Origin',(-2.,9.6,5.));
#10347=CARTESIAN_POINT('Origin',(-2.,8.5,5.));
#10348=CARTESIAN_POINT('',(-2.8,8.5,5.));
#10349=CARTESIAN_POINT('Origin',(-2.,8.5,5.));
#10350=CARTESIAN_POINT('',(-2.5,8.5,5.));
#10351=CARTESIAN_POINT('Origin',(-2.,8.5,5.));
#10352=CARTESIAN_POINT('Origin',(-2.,8.2,5.));
#10353=CARTESIAN_POINT('',(-2.8,8.2,5.));
#10354=CARTESIAN_POINT('',(-2.8,8.2,5.));
#10355=CARTESIAN_POINT('Origin',(-2.,8.2,5.));
#10356=CARTESIAN_POINT('Origin',(-2.,8.2,5.));
#10357=CARTESIAN_POINT('Origin',(-2.,8.5,5.));
#10358=CARTESIAN_POINT('',(-2.5,10.8,5.));
#10359=CARTESIAN_POINT('Origin',(-2.,10.8,5.));
#10360=CARTESIAN_POINT('',(-2.5,8.5,5.));
#10361=CARTESIAN_POINT('Origin',(-2.,10.8,5.));
#11669=UNCERTAINTY_MEASURE_WITH_UNIT(LENGTH_MEASURE(0.001),#11749,
'DISTANCE_ACCURACY_VALUE',
'Maximum model space distance between geometric entities at asserted c
onnectivities');
#11699=UNCERTAINTY_MEASURE_WITH_UNIT(LENGTH_MEASURE(0.001),#11749,
'DISTANCE_ACCURACY_VALUE',
'Maximum model space distance between geometric entities at asserted c
onnectivities');
#11718=(
GEOMETRIC_REPRESENTATION_CONTEXT(3)
GLOBAL_UNCERTAINTY_ASSIGNED_CONTEXT((#11669))
GLOBAL_UNIT_ASSIGNED_CONTEXT((#11749,#11751,#11752))
REPRESENTATION_CONTEXT('','3D')
);
#11748=(
GEOMETRIC_REPRESENTATION_CONTEXT(3)
GLOBAL_UNCERTAINTY_ASSIGNED_CONTEXT((#11699))
GLOBAL_UNIT_ASSIGNED_CONTEXT((#11749,#11751,#11752))
REPRESENTATION_CONTEXT('','3D')
);
#11749=(
LENGTH_UNIT()
NAMED_UNIT(*)
SI_UNIT(.CENTI.,.METRE.)
);
#11751=(
NAMED_UNIT(*)
PLANE_ANGLE_UNIT()
SI_UNIT($,.RADIAN.)
);
#11752=(
NAMED_UNIT(*)
SI_UNIT($,.STERADIAN.)
SOLID_ANGLE_UNIT()
);
#11771=SHAPE_DEFINITION_REPRESENTATION(#11819,#11942);
#11819=PRODUCT_DEFINITION_SHAPE('',$,#11991);
#11942=SHAPE_REPRESENTATION('',(#7022),#11718);
#11972=PRODUCT_DEFINITION_CONTEXT('part definition',#12118,'design');
#11991=PRODUCT_DEFINITION('Dead axle_2','Dead axle (2)',#12039,#11972);
#12039=PRODUCT_DEFINITION_FORMATION('',$,#12138);
#12118=APPLICATION_CONTEXT(
'Core Data for Automotive Mechanical Design Process');
#12119=PRODUCT_CONTEXT('part definition',#12118,'mechanical');
#12138=PRODUCT('Dead axle_2','Dead axle (2)','Dead axle',(#12119));
#12169=PRESENTATION_STYLE_ASSIGNMENT((#12174));
#12174=SURFACE_STYLE_USAGE(.BOTH.,#12179);
#12179=SURFACE_SIDE_STYLE('',(#12184));
#12184=SURFACE_STYLE_FILL_AREA(#12189);
#12189=FILL_AREA_STYLE('CAD Library Painted - Engineering blue',(#12194));
#12194=FILL_AREA_STYLE_COLOUR('CAD Library Painted - Engineering blue',
#12199);
#12199=COLOUR_RGB('CAD Library Painted - Engineering blue',0.12156862745098,
0.356862745098039,0.6);
ENDSEC;
END-ISO-10303-21;
